ISO-10303-21;
HEADER;
/* Generated by software containing ST-Developer
 * from STEP Tools, Inc. (www.steptools.com) 
 */

FILE_DESCRIPTION(
/* description */ ('STEP AP214'),
/* implementation_level */ '2;1');

FILE_NAME(
/* name */ 'Ball Screw Shaft.step',
/* time_stamp */ '2026-11-15T14:55:55-08:00',
/* author */ (''),
/* organization */ (''),
/* preprocessor_version */ 'ST-DEVELOPER v20.2',
/* originating_system */ 'Autodesk Translation Framework v15.17.0.0',
/* authorisation */ '');

FILE_SCHEMA (('AUTOMOTIVE_DESIGN { 1 0 10303 214 3 1 1 }'));
ENDSEC;

DATA;
#10=MECHANICAL_DESIGN_GEOMETRIC_PRESENTATION_REPRESENTATION('',(#927),#57079);
#636=TOROIDAL_SURFACE('',#24942,5.2000000000001,0.199999999999989);
#637=TOROIDAL_SURFACE('',#24950,6.30000000000001,0.300000000000011);
#638=TOROIDAL_SURFACE('',#24961,5.3,0.3);
#649=B_SPLINE_CURVE_WITH_KNOTS('',3,(#34781,#34782,#34783,#34784,#34785,
#34786,#34787,#34788,#34789,#34790,#34791,#34792,#34793,#34794,#34795,#34796,
#34797,#34798),.UNSPECIFIED.,.F.,.F.,(4,2,2,2,2,2,2,2,4),(0.,0.0568915880983864,
0.113783176196773,0.170657815990574,0.227532455784374,0.284407095578175,
0.341281735371975,0.398173323470362,0.455064911568748),.UNSPECIFIED.);
#650=B_SPLINE_CURVE_WITH_KNOTS('',3,(#34871,#34872,#34873,#34874),
 .UNSPECIFIED.,.F.,.F.,(4,4),(0.00307564709988169,0.0038021193092735),
 .UNSPECIFIED.);
#651=B_SPLINE_CURVE_WITH_KNOTS('',3,(#34877,#34878,#34879,#34880),
 .UNSPECIFIED.,.F.,.F.,(4,4),(0.00334106894839127,0.00406713764756004),
 .UNSPECIFIED.);
#869=SHAPE_REPRESENTATION_RELATIONSHIP('SRR','None',#57253,#898);
#898=ADVANCED_BREP_SHAPE_REPRESENTATION('',(#964),#57045);
#927=STYLED_ITEM('',(#57444),#964);
#964=MANIFOLD_SOLID_BREP('Body1',#24527);
#1020=FACE_BOUND('',#3594,.T.);
#1021=FACE_BOUND('',#3596,.T.);
#1022=FACE_BOUND('',#3598,.T.);
#1023=FACE_BOUND('',#3600,.T.);
#1024=FACE_BOUND('',#3602,.T.);
#1352=PLANE('',#24976);
#1353=PLANE('',#24977);
#1354=PLANE('',#24978);
#1355=PLANE('',#24979);
#1356=PLANE('',#24980);
#1357=PLANE('',#24983);
#1358=PLANE('',#24984);
#1359=PLANE('',#24985);
#1360=PLANE('',#24986);
#1361=PLANE('',#24987);
#2109=CONICAL_SURFACE('',#24945,5.50000000000001,0.785398163397526);
#2110=CONICAL_SURFACE('',#24953,7.00000000000006,0.785398163397535);
#2111=CONICAL_SURFACE('',#24959,7.49999999999999,0.785398163397418);
#2112=CONICAL_SURFACE('',#24974,5.,0.785398163397416);
#2113=CONICAL_SURFACE('',#24981,4.50000000000006,0.78539816339741);
#2185=FACE_OUTER_BOUND('',#3580,.T.);
#2186=FACE_OUTER_BOUND('',#3581,.T.);
#2187=FACE_OUTER_BOUND('',#3582,.T.);
#2188=FACE_OUTER_BOUND('',#3583,.T.);
#2189=FACE_OUTER_BOUND('',#3584,.T.);
#2190=FACE_OUTER_BOUND('',#3585,.T.);
#2191=FACE_OUTER_BOUND('',#3586,.T.);
#2192=FACE_OUTER_BOUND('',#3587,.T.);
#2193=FACE_OUTER_BOUND('',#3588,.T.);
#2194=FACE_OUTER_BOUND('',#3589,.T.);
#2195=FACE_OUTER_BOUND('',#3590,.T.);
#2196=FACE_OUTER_BOUND('',#3591,.T.);
#2197=FACE_OUTER_BOUND('',#3592,.T.);
#2198=FACE_OUTER_BOUND('',#3593,.T.);
#2199=FACE_OUTER_BOUND('',#3595,.T.);
#2200=FACE_OUTER_BOUND('',#3597,.T.);
#2201=FACE_OUTER_BOUND('',#3599,.T.);
#2202=FACE_OUTER_BOUND('',#3601,.T.);
#2203=FACE_OUTER_BOUND('',#3603,.T.);
#2204=FACE_OUTER_BOUND('',#3604,.T.);
#2205=FACE_OUTER_BOUND('',#3605,.T.);
#2206=FACE_OUTER_BOUND('',#3606,.T.);
#2207=FACE_OUTER_BOUND('',#3607,.T.);
#2208=FACE_OUTER_BOUND('',#3608,.T.);
#2209=FACE_OUTER_BOUND('',#3609,.T.);
#3580=EDGE_LOOP('',(#16044,#16045,#16046,#16047,#16048,#16049,#16050,#16051));
#3581=EDGE_LOOP('',(#16052,#16053,#16054,#16055));
#3582=EDGE_LOOP('',(#16056,#16057,#16058,#16059));
#3583=EDGE_LOOP('',(#16060,#16061,#16062,#16063));
#3584=EDGE_LOOP('',(#16064,#16065,#16066,#16067));
#3585=EDGE_LOOP('',(#16068,#16069,#16070,#16071));
#3586=EDGE_LOOP('',(#16072,#16073,#16074,#16075,#16076));
#3587=EDGE_LOOP('',(#16077,#16078,#16079,#16080,#16081));
#3588=EDGE_LOOP('',(#16082,#16083,#16084,#16085));
#3589=EDGE_LOOP('',(#16086,#16087,#16088,#16089));
#3590=EDGE_LOOP('',(#16090,#16091,#16092,#16093));
#3591=EDGE_LOOP('',(#16094,#16095,#16096,#16097,#16098));
#3592=EDGE_LOOP('',(#16099,#16100,#16101,#16102,#16103));
#3593=EDGE_LOOP('',(#16104));
#3594=EDGE_LOOP('',(#16105));
#3595=EDGE_LOOP('',(#16106));
#3596=EDGE_LOOP('',(#16107));
#3597=EDGE_LOOP('',(#16108));
#3598=EDGE_LOOP('',(#16109));
#3599=EDGE_LOOP('',(#16110));
#3600=EDGE_LOOP('',(#16111));
#3601=EDGE_LOOP('',(#16112));
#3602=EDGE_LOOP('',(#16113));
#3603=EDGE_LOOP('',(#16114,#16115,#16116,#16117,#16118));
#3604=EDGE_LOOP('',(#16119,#16120,#16121,#16122));
#3605=EDGE_LOOP('',(#16123));
#3606=EDGE_LOOP('',(#16124,#16125,#16126,#16127,#16128));
#3607=EDGE_LOOP('',(#16129,#16130,#16131,#16132,#16133));
#3608=EDGE_LOOP('',(#16134,#16135,#16136,#16137));
#3609=EDGE_LOOP('',(#16138,#16139,#16140,#16141));
#5291=LINE('',#34775,#7258);
#5292=LINE('',#34779,#7259);
#5293=LINE('',#34800,#7260);
#5294=LINE('',#34810,#7261);
#5295=LINE('',#34815,#7262);
#5296=LINE('',#34824,#7263);
#5297=LINE('',#34831,#7264);
#5298=LINE('',#34834,#7265);
#5299=LINE('',#34845,#7266);
#5300=LINE('',#34850,#7267);
#5301=LINE('',#34858,#7268);
#5302=LINE('',#34862,#7269);
#5303=LINE('',#34883,#7270);
#5304=LINE('',#34885,#7271);
#5305=LINE('',#34886,#7272);
#5306=LINE('',#34890,#7273);
#5307=LINE('',#34891,#7274);
#5308=LINE('',#34894,#7275);
#5309=LINE('',#34895,#7276);
#7258=VECTOR('',#27631,5.00000000000009);
#7259=VECTOR('',#27634,1000.);
#7260=VECTOR('',#27635,1000.);
#7261=VECTOR('',#27648,5.50000000000001);
#7262=VECTOR('',#27655,6.00000000000005);
#7263=VECTOR('',#27666,7.00000000000006);
#7264=VECTOR('',#27675,7.50000000000004);
#7265=VECTOR('',#27678,7.49999999999999);
#7266=VECTOR('',#27693,5.);
#7267=VECTOR('',#27698,4.8);
#7268=VECTOR('',#27707,5.);
#7269=VECTOR('',#27712,5.);
#7270=VECTOR('',#27731,1000.);
#7271=VECTOR('',#27732,1000.);
#7272=VECTOR('',#27733,1000.);
#7273=VECTOR('',#27738,1000.);
#7274=VECTOR('',#27739,1000.);
#7275=VECTOR('',#27742,1000.);
#7276=VECTOR('',#27743,1000.);
#9209=CIRCLE('',#24939,5.0000000000001);
#9210=CIRCLE('',#24940,5.00000000000007);
#9211=CIRCLE('',#24941,5.00000000000007);
#9212=CIRCLE('',#24943,5.2000000000001);
#9213=CIRCLE('',#24944,0.199999999999989);
#9214=CIRCLE('',#24946,6.00000000000009);
#9215=CIRCLE('',#24947,5.50000000000001);
#9216=CIRCLE('',#24949,6.00000000000001);
#9217=CIRCLE('',#24951,6.30000000000001);
#9218=CIRCLE('',#24952,0.300000000000011);
#9219=CIRCLE('',#24954,7.50000000000009);
#9220=CIRCLE('',#24955,7.00000000000006);
#9221=CIRCLE('',#24957,7.49999999999999);
#9222=CIRCLE('',#24958,7.49999999999999);
#9223=CIRCLE('',#24960,7.00000000000002);
#9224=CIRCLE('',#24962,5.);
#9225=CIRCLE('',#24963,0.3);
#9226=CIRCLE('',#24964,5.3);
#9227=CIRCLE('',#24966,5.);
#9228=CIRCLE('',#24968,4.8);
#9229=CIRCLE('',#24969,4.8);
#9230=CIRCLE('',#24971,5.);
#9231=CIRCLE('',#24972,5.);
#9232=CIRCLE('',#24973,5.);
#9233=CIRCLE('',#24975,4.50000000000003);
#9234=CIRCLE('',#24982,4.50000000000006);
#9235=CIRCLE('',#24988,1.5);
#10323=VERTEX_POINT('',#34772);
#10324=VERTEX_POINT('',#34774);
#10325=VERTEX_POINT('',#34776);
#10326=VERTEX_POINT('',#34778);
#10327=VERTEX_POINT('',#34780);
#10328=VERTEX_POINT('',#34799);
#10329=VERTEX_POINT('',#34803);
#10330=VERTEX_POINT('',#34807);
#10331=VERTEX_POINT('',#34809);
#10332=VERTEX_POINT('',#34813);
#10333=VERTEX_POINT('',#34817);
#10334=VERTEX_POINT('',#34821);
#10335=VERTEX_POINT('',#34823);
#10336=VERTEX_POINT('',#34827);
#10337=VERTEX_POINT('',#34828);
#10338=VERTEX_POINT('',#34833);
#10339=VERTEX_POINT('',#34837);
#10340=VERTEX_POINT('',#34839);
#10341=VERTEX_POINT('',#34843);
#10342=VERTEX_POINT('',#34847);
#10343=VERTEX_POINT('',#34849);
#10344=VERTEX_POINT('',#34853);
#10345=VERTEX_POINT('',#34854);
#10346=VERTEX_POINT('',#34857);
#10347=VERTEX_POINT('',#34861);
#10348=VERTEX_POINT('',#34870);
#10349=VERTEX_POINT('',#34875);
#10350=VERTEX_POINT('',#34882);
#10351=VERTEX_POINT('',#34884);
#10352=VERTEX_POINT('',#34889);
#10353=VERTEX_POINT('',#34893);
#12567=EDGE_CURVE('',#10323,#10323,#9209,.T.);
#12568=EDGE_CURVE('',#10323,#10324,#5291,.T.);
#12569=EDGE_CURVE('',#10324,#10325,#9210,.T.);
#12570=EDGE_CURVE('',#10325,#10326,#5292,.T.);
#12571=EDGE_CURVE('',#10326,#10327,#649,.F.);
#12572=EDGE_CURVE('',#10327,#10328,#5293,.T.);
#12573=EDGE_CURVE('',#10328,#10324,#9211,.T.);
#12574=EDGE_CURVE('',#10329,#10329,#9212,.T.);
#12575=EDGE_CURVE('',#10329,#10323,#9213,.T.);
#12576=EDGE_CURVE('',#10330,#10330,#9214,.T.);
#12577=EDGE_CURVE('',#10330,#10331,#5294,.T.);
#12578=EDGE_CURVE('',#10331,#10331,#9215,.T.);
#12579=EDGE_CURVE('',#10332,#10332,#9216,.T.);
#12580=EDGE_CURVE('',#10332,#10330,#5295,.T.);
#12581=EDGE_CURVE('',#10333,#10333,#9217,.T.);
#12582=EDGE_CURVE('',#10333,#10332,#9218,.T.);
#12583=EDGE_CURVE('',#10334,#10334,#9219,.T.);
#12584=EDGE_CURVE('',#10334,#10335,#5296,.T.);
#12585=EDGE_CURVE('',#10335,#10335,#9220,.T.);
#12586=EDGE_CURVE('',#10336,#10337,#9221,.T.);
#12587=EDGE_CURVE('',#10337,#10336,#9222,.T.);
#12588=EDGE_CURVE('',#10337,#10334,#5297,.T.);
#12589=EDGE_CURVE('',#10336,#10338,#5298,.T.);
#12590=EDGE_CURVE('',#10338,#10338,#9223,.T.);
#12591=EDGE_CURVE('',#10339,#10339,#9224,.T.);
#12592=EDGE_CURVE('',#10339,#10340,#9225,.T.);
#12593=EDGE_CURVE('',#10340,#10340,#9226,.T.);
#12594=EDGE_CURVE('',#10341,#10341,#9227,.T.);
#12595=EDGE_CURVE('',#10341,#10339,#5299,.T.);
#12596=EDGE_CURVE('',#10342,#10342,#9228,.T.);
#12597=EDGE_CURVE('',#10342,#10343,#5300,.T.);
#12598=EDGE_CURVE('',#10343,#10343,#9229,.T.);
#12599=EDGE_CURVE('',#10344,#10345,#9230,.T.);
#12600=EDGE_CURVE('',#10345,#10344,#9231,.T.);
#12601=EDGE_CURVE('',#10345,#10346,#5301,.T.);
#12602=EDGE_CURVE('',#10346,#10346,#9232,.T.);
#12603=EDGE_CURVE('',#10344,#10347,#5302,.T.);
#12604=EDGE_CURVE('',#10347,#10347,#9233,.T.);
#12605=EDGE_CURVE('',#10328,#10348,#650,.T.);
#12606=EDGE_CURVE('',#10348,#10349,#9234,.T.);
#12607=EDGE_CURVE('',#10349,#10325,#651,.T.);
#12608=EDGE_CURVE('',#10350,#10348,#5303,.T.);
#12609=EDGE_CURVE('',#10351,#10350,#5304,.T.);
#12610=EDGE_CURVE('',#10351,#10349,#5305,.T.);
#12611=EDGE_CURVE('',#10327,#10352,#5306,.T.);
#12612=EDGE_CURVE('',#10352,#10350,#5307,.T.);
#12613=EDGE_CURVE('',#10353,#10351,#5308,.T.);
#12614=EDGE_CURVE('',#10353,#10326,#5309,.T.);
#12615=EDGE_CURVE('',#10352,#10353,#9235,.T.);
#16044=ORIENTED_EDGE('',*,*,#12567,.F.);
#16045=ORIENTED_EDGE('',*,*,#12568,.T.);
#16046=ORIENTED_EDGE('',*,*,#12569,.T.);
#16047=ORIENTED_EDGE('',*,*,#12570,.T.);
#16048=ORIENTED_EDGE('',*,*,#12571,.T.);
#16049=ORIENTED_EDGE('',*,*,#12572,.T.);
#16050=ORIENTED_EDGE('',*,*,#12573,.T.);
#16051=ORIENTED_EDGE('',*,*,#12568,.F.);
#16052=ORIENTED_EDGE('',*,*,#12574,.F.);
#16053=ORIENTED_EDGE('',*,*,#12575,.T.);
#16054=ORIENTED_EDGE('',*,*,#12567,.T.);
#16055=ORIENTED_EDGE('',*,*,#12575,.F.);
#16056=ORIENTED_EDGE('',*,*,#12576,.F.);
#16057=ORIENTED_EDGE('',*,*,#12577,.T.);
#16058=ORIENTED_EDGE('',*,*,#12578,.T.);
#16059=ORIENTED_EDGE('',*,*,#12577,.F.);
#16060=ORIENTED_EDGE('',*,*,#12579,.F.);
#16061=ORIENTED_EDGE('',*,*,#12580,.T.);
#16062=ORIENTED_EDGE('',*,*,#12576,.T.);
#16063=ORIENTED_EDGE('',*,*,#12580,.F.);
#16064=ORIENTED_EDGE('',*,*,#12581,.F.);
#16065=ORIENTED_EDGE('',*,*,#12582,.T.);
#16066=ORIENTED_EDGE('',*,*,#12579,.T.);
#16067=ORIENTED_EDGE('',*,*,#12582,.F.);
#16068=ORIENTED_EDGE('',*,*,#12583,.F.);
#16069=ORIENTED_EDGE('',*,*,#12584,.T.);
#16070=ORIENTED_EDGE('',*,*,#12585,.T.);
#16071=ORIENTED_EDGE('',*,*,#12584,.F.);
#16072=ORIENTED_EDGE('',*,*,#12586,.F.);
#16073=ORIENTED_EDGE('',*,*,#12587,.F.);
#16074=ORIENTED_EDGE('',*,*,#12588,.T.);
#16075=ORIENTED_EDGE('',*,*,#12583,.T.);
#16076=ORIENTED_EDGE('',*,*,#12588,.F.);
#16077=ORIENTED_EDGE('',*,*,#12586,.T.);
#16078=ORIENTED_EDGE('',*,*,#12587,.T.);
#16079=ORIENTED_EDGE('',*,*,#12589,.T.);
#16080=ORIENTED_EDGE('',*,*,#12590,.F.);
#16081=ORIENTED_EDGE('',*,*,#12589,.F.);
#16082=ORIENTED_EDGE('',*,*,#12591,.F.);
#16083=ORIENTED_EDGE('',*,*,#12592,.T.);
#16084=ORIENTED_EDGE('',*,*,#12593,.T.);
#16085=ORIENTED_EDGE('',*,*,#12592,.F.);
#16086=ORIENTED_EDGE('',*,*,#12594,.F.);
#16087=ORIENTED_EDGE('',*,*,#12595,.T.);
#16088=ORIENTED_EDGE('',*,*,#12591,.T.);
#16089=ORIENTED_EDGE('',*,*,#12595,.F.);
#16090=ORIENTED_EDGE('',*,*,#12596,.F.);
#16091=ORIENTED_EDGE('',*,*,#12597,.T.);
#16092=ORIENTED_EDGE('',*,*,#12598,.T.);
#16093=ORIENTED_EDGE('',*,*,#12597,.F.);
#16094=ORIENTED_EDGE('',*,*,#12599,.F.);
#16095=ORIENTED_EDGE('',*,*,#12600,.F.);
#16096=ORIENTED_EDGE('',*,*,#12601,.T.);
#16097=ORIENTED_EDGE('',*,*,#12602,.T.);
#16098=ORIENTED_EDGE('',*,*,#12601,.F.);
#16099=ORIENTED_EDGE('',*,*,#12599,.T.);
#16100=ORIENTED_EDGE('',*,*,#12600,.T.);
#16101=ORIENTED_EDGE('',*,*,#12603,.T.);
#16102=ORIENTED_EDGE('',*,*,#12604,.F.);
#16103=ORIENTED_EDGE('',*,*,#12603,.F.);
#16104=ORIENTED_EDGE('',*,*,#12602,.F.);
#16105=ORIENTED_EDGE('',*,*,#12596,.T.);
#16106=ORIENTED_EDGE('',*,*,#12594,.T.);
#16107=ORIENTED_EDGE('',*,*,#12598,.F.);
#16108=ORIENTED_EDGE('',*,*,#12590,.T.);
#16109=ORIENTED_EDGE('',*,*,#12593,.F.);
#16110=ORIENTED_EDGE('',*,*,#12585,.F.);
#16111=ORIENTED_EDGE('',*,*,#12581,.T.);
#16112=ORIENTED_EDGE('',*,*,#12578,.F.);
#16113=ORIENTED_EDGE('',*,*,#12574,.T.);
#16114=ORIENTED_EDGE('',*,*,#12573,.F.);
#16115=ORIENTED_EDGE('',*,*,#12605,.T.);
#16116=ORIENTED_EDGE('',*,*,#12606,.T.);
#16117=ORIENTED_EDGE('',*,*,#12607,.T.);
#16118=ORIENTED_EDGE('',*,*,#12569,.F.);
#16119=ORIENTED_EDGE('',*,*,#12606,.F.);
#16120=ORIENTED_EDGE('',*,*,#12608,.F.);
#16121=ORIENTED_EDGE('',*,*,#12609,.F.);
#16122=ORIENTED_EDGE('',*,*,#12610,.T.);
#16123=ORIENTED_EDGE('',*,*,#12604,.T.);
#16124=ORIENTED_EDGE('',*,*,#12572,.F.);
#16125=ORIENTED_EDGE('',*,*,#12611,.T.);
#16126=ORIENTED_EDGE('',*,*,#12612,.T.);
#16127=ORIENTED_EDGE('',*,*,#12608,.T.);
#16128=ORIENTED_EDGE('',*,*,#12605,.F.);
#16129=ORIENTED_EDGE('',*,*,#12613,.F.);
#16130=ORIENTED_EDGE('',*,*,#12614,.T.);
#16131=ORIENTED_EDGE('',*,*,#12570,.F.);
#16132=ORIENTED_EDGE('',*,*,#12607,.F.);
#16133=ORIENTED_EDGE('',*,*,#12610,.F.);
#16134=ORIENTED_EDGE('',*,*,#12615,.T.);
#16135=ORIENTED_EDGE('',*,*,#12613,.T.);
#16136=ORIENTED_EDGE('',*,*,#12609,.T.);
#16137=ORIENTED_EDGE('',*,*,#12612,.F.);
#16138=ORIENTED_EDGE('',*,*,#12611,.F.);
#16139=ORIENTED_EDGE('',*,*,#12571,.F.);
#16140=ORIENTED_EDGE('',*,*,#12614,.F.);
#16141=ORIENTED_EDGE('',*,*,#12615,.F.);
#22754=CYLINDRICAL_SURFACE('',#24938,5.00000000000009);
#22755=CYLINDRICAL_SURFACE('',#24948,6.00000000000005);
#22756=CYLINDRICAL_SURFACE('',#24956,7.50000000000004);
#22757=CYLINDRICAL_SURFACE('',#24965,5.);
#22758=CYLINDRICAL_SURFACE('',#24967,4.8);
#22759=CYLINDRICAL_SURFACE('',#24970,5.);
#22760=CYLINDRICAL_SURFACE('',#24989,1.5);
#23177=ADVANCED_FACE('',(#2185),#22754,.T.);
#23178=ADVANCED_FACE('',(#2186),#636,.F.);
#23179=ADVANCED_FACE('',(#2187),#2109,.T.);
#23180=ADVANCED_FACE('',(#2188),#22755,.T.);
#23181=ADVANCED_FACE('',(#2189),#637,.F.);
#23182=ADVANCED_FACE('',(#2190),#2110,.T.);
#23183=ADVANCED_FACE('',(#2191),#22756,.T.);
#23184=ADVANCED_FACE('',(#2192),#2111,.T.);
#23185=ADVANCED_FACE('',(#2193),#638,.F.);
#23186=ADVANCED_FACE('',(#2194),#22757,.T.);
#23187=ADVANCED_FACE('',(#2195),#22758,.T.);
#23188=ADVANCED_FACE('',(#2196),#22759,.T.);
#23189=ADVANCED_FACE('',(#2197),#2112,.T.);
#23190=ADVANCED_FACE('',(#2198,#1020),#1352,.F.);
#23191=ADVANCED_FACE('',(#2199,#1021),#1353,.F.);
#23192=ADVANCED_FACE('',(#2200,#1022),#1354,.F.);
#23193=ADVANCED_FACE('',(#2201,#1023),#1355,.F.);
#23194=ADVANCED_FACE('',(#2202,#1024),#1356,.F.);
#23195=ADVANCED_FACE('',(#2203),#2113,.T.);
#23196=ADVANCED_FACE('',(#2204),#1357,.F.);
#23197=ADVANCED_FACE('',(#2205),#1358,.F.);
#23198=ADVANCED_FACE('',(#2206),#1359,.F.);
#23199=ADVANCED_FACE('',(#2207),#1360,.F.);
#23200=ADVANCED_FACE('',(#2208),#1361,.F.);
#23201=ADVANCED_FACE('',(#2209),#22760,.F.);
#24527=CLOSED_SHELL('',(#23177,#23178,#23179,#23180,#23181,#23182,#23183,
#23184,#23185,#23186,#23187,#23188,#23189,#23190,#23191,#23192,#23193,#23194,
#23195,#23196,#23197,#23198,#23199,#23200,#23201));
#24937=AXIS2_PLACEMENT_3D('',#34770,#27625,#27626);
#24938=AXIS2_PLACEMENT_3D('',#34771,#27627,#27628);
#24939=AXIS2_PLACEMENT_3D('',#34773,#27629,#27630);
#24940=AXIS2_PLACEMENT_3D('',#34777,#27632,#27633);
#24941=AXIS2_PLACEMENT_3D('',#34801,#27636,#27637);
#24942=AXIS2_PLACEMENT_3D('',#34802,#27638,#27639);
#24943=AXIS2_PLACEMENT_3D('',#34804,#27640,#27641);
#24944=AXIS2_PLACEMENT_3D('',#34805,#27642,#27643);
#24945=AXIS2_PLACEMENT_3D('',#34806,#27644,#27645);
#24946=AXIS2_PLACEMENT_3D('',#34808,#27646,#27647);
#24947=AXIS2_PLACEMENT_3D('',#34811,#27649,#27650);
#24948=AXIS2_PLACEMENT_3D('',#34812,#27651,#27652);
#24949=AXIS2_PLACEMENT_3D('',#34814,#27653,#27654);
#24950=AXIS2_PLACEMENT_3D('',#34816,#27656,#27657);
#24951=AXIS2_PLACEMENT_3D('',#34818,#27658,#27659);
#24952=AXIS2_PLACEMENT_3D('',#34819,#27660,#27661);
#24953=AXIS2_PLACEMENT_3D('',#34820,#27662,#27663);
#24954=AXIS2_PLACEMENT_3D('',#34822,#27664,#27665);
#24955=AXIS2_PLACEMENT_3D('',#34825,#27667,#27668);
#24956=AXIS2_PLACEMENT_3D('',#34826,#27669,#27670);
#24957=AXIS2_PLACEMENT_3D('',#34829,#27671,#27672);
#24958=AXIS2_PLACEMENT_3D('',#34830,#27673,#27674);
#24959=AXIS2_PLACEMENT_3D('',#34832,#27676,#27677);
#24960=AXIS2_PLACEMENT_3D('',#34835,#27679,#27680);
#24961=AXIS2_PLACEMENT_3D('',#34836,#27681,#27682);
#24962=AXIS2_PLACEMENT_3D('',#34838,#27683,#27684);
#24963=AXIS2_PLACEMENT_3D('',#34840,#27685,#27686);
#24964=AXIS2_PLACEMENT_3D('',#34841,#27687,#27688);
#24965=AXIS2_PLACEMENT_3D('',#34842,#27689,#27690);
#24966=AXIS2_PLACEMENT_3D('',#34844,#27691,#27692);
#24967=AXIS2_PLACEMENT_3D('',#34846,#27694,#27695);
#24968=AXIS2_PLACEMENT_3D('',#34848,#27696,#27697);
#24969=AXIS2_PLACEMENT_3D('',#34851,#27699,#27700);
#24970=AXIS2_PLACEMENT_3D('',#34852,#27701,#27702);
#24971=AXIS2_PLACEMENT_3D('',#34855,#27703,#27704);
#24972=AXIS2_PLACEMENT_3D('',#34856,#27705,#27706);
#24973=AXIS2_PLACEMENT_3D('',#34859,#27708,#27709);
#24974=AXIS2_PLACEMENT_3D('',#34860,#27710,#27711);
#24975=AXIS2_PLACEMENT_3D('',#34863,#27713,#27714);
#24976=AXIS2_PLACEMENT_3D('',#34864,#27715,#27716);
#24977=AXIS2_PLACEMENT_3D('',#34865,#27717,#27718);
#24978=AXIS2_PLACEMENT_3D('',#34866,#27719,#27720);
#24979=AXIS2_PLACEMENT_3D('',#34867,#27721,#27722);
#24980=AXIS2_PLACEMENT_3D('',#34868,#27723,#27724);
#24981=AXIS2_PLACEMENT_3D('',#34869,#27725,#27726);
#24982=AXIS2_PLACEMENT_3D('',#34876,#27727,#27728);
#24983=AXIS2_PLACEMENT_3D('',#34881,#27729,#27730);
#24984=AXIS2_PLACEMENT_3D('',#34887,#27734,#27735);
#24985=AXIS2_PLACEMENT_3D('',#34888,#27736,#27737);
#24986=AXIS2_PLACEMENT_3D('',#34892,#27740,#27741);
#24987=AXIS2_PLACEMENT_3D('',#34896,#27744,#27745);
#24988=AXIS2_PLACEMENT_3D('',#34897,#27746,#27747);
#24989=AXIS2_PLACEMENT_3D('',#34898,#27748,#27749);
#27625=DIRECTION('axis',(0.,0.,1.));
#27626=DIRECTION('refdir',(1.,0.,0.));
#27627=DIRECTION('center_axis',(-1.,0.,0.));
#27628=DIRECTION('ref_axis',(0.,0.,1.));
#27629=DIRECTION('center_axis',(-1.,0.,0.));
#27630=DIRECTION('ref_axis',(0.,0.,1.));
#27631=DIRECTION('',(1.,0.,0.));
#27632=DIRECTION('center_axis',(-1.,0.,0.));
#27633=DIRECTION('ref_axis',(0.,0.,1.));
#27634=DIRECTION('',(-1.,0.,0.));
#27635=DIRECTION('',(1.,0.,0.));
#27636=DIRECTION('center_axis',(-1.,0.,0.));
#27637=DIRECTION('ref_axis',(0.,0.,1.));
#27638=DIRECTION('center_axis',(-1.,0.,0.));
#27639=DIRECTION('ref_axis',(0.,0.,1.));
#27640=DIRECTION('center_axis',(-1.,0.,0.));
#27641=DIRECTION('ref_axis',(0.,0.,1.));
#27642=DIRECTION('center_axis',(0.,1.,-1.22464679914735E-16));
#27643=DIRECTION('ref_axis',(0.,-1.22464679914735E-16,-1.));
#27644=DIRECTION('center_axis',(-1.,0.,0.));
#27645=DIRECTION('ref_axis',(0.,0.,1.));
#27646=DIRECTION('center_axis',(-1.,0.,0.));
#27647=DIRECTION('ref_axis',(0.,0.,1.));
#27648=DIRECTION('',(0.707106781186492,8.65956056235561E-17,0.707106781186603));
#27649=DIRECTION('center_axis',(-1.,0.,0.));
#27650=DIRECTION('ref_axis',(0.,0.,1.));
#27651=DIRECTION('center_axis',(-1.,0.,0.));
#27652=DIRECTION('ref_axis',(0.,0.,1.));
#27653=DIRECTION('center_axis',(-1.,0.,0.));
#27654=DIRECTION('ref_axis',(0.,0.,1.));
#27655=DIRECTION('',(1.,0.,0.));
#27656=DIRECTION('center_axis',(-1.,0.,0.));
#27657=DIRECTION('ref_axis',(0.,0.,1.));
#27658=DIRECTION('center_axis',(-1.,0.,0.));
#27659=DIRECTION('ref_axis',(0.,0.,1.));
#27660=DIRECTION('center_axis',(0.,1.,-1.22464679914735E-16));
#27661=DIRECTION('ref_axis',(0.,-1.22464679914735E-16,-1.));
#27662=DIRECTION('center_axis',(-1.,0.,0.));
#27663=DIRECTION('ref_axis',(0.,0.,1.));
#27664=DIRECTION('center_axis',(-1.,0.,0.));
#27665=DIRECTION('ref_axis',(0.,0.,1.));
#27666=DIRECTION('',(0.707106781186486,8.65956056235568E-17,0.707106781186609));
#27667=DIRECTION('center_axis',(-1.,0.,0.));
#27668=DIRECTION('ref_axis',(0.,0.,1.));
#27669=DIRECTION('center_axis',(-1.,0.,0.));
#27670=DIRECTION('ref_axis',(0.,0.,1.));
#27671=DIRECTION('center_axis',(-1.,0.,0.));
#27672=DIRECTION('ref_axis',(0.,0.,1.));
#27673=DIRECTION('center_axis',(-1.,0.,0.));
#27674=DIRECTION('ref_axis',(0.,0.,1.));
#27675=DIRECTION('',(1.,0.,0.));
#27676=DIRECTION('center_axis',(1.,0.,0.));
#27677=DIRECTION('ref_axis',(0.,0.,-1.));
#27678=DIRECTION('',(-0.707106781186569,8.65956056235467E-17,-0.707106781186526));
#27679=DIRECTION('center_axis',(-1.,0.,0.));
#27680=DIRECTION('ref_axis',(0.,0.,1.));
#27681=DIRECTION('center_axis',(-1.,0.,0.));
#27682=DIRECTION('ref_axis',(0.,0.,1.));
#27683=DIRECTION('center_axis',(-1.,0.,0.));
#27684=DIRECTION('ref_axis',(0.,0.,1.));
#27685=DIRECTION('center_axis',(0.,1.,-1.22464679914735E-16));
#27686=DIRECTION('ref_axis',(0.,-1.22464679914735E-16,-1.));
#27687=DIRECTION('center_axis',(-1.,0.,0.));
#27688=DIRECTION('ref_axis',(0.,0.,1.));
#27689=DIRECTION('center_axis',(-1.,0.,0.));
#27690=DIRECTION('ref_axis',(0.,0.,1.));
#27691=DIRECTION('center_axis',(-1.,0.,0.));
#27692=DIRECTION('ref_axis',(0.,0.,1.));
#27693=DIRECTION('',(1.,0.,0.));
#27694=DIRECTION('center_axis',(-1.,0.,0.));
#27695=DIRECTION('ref_axis',(0.,0.,1.));
#27696=DIRECTION('center_axis',(-1.,0.,0.));
#27697=DIRECTION('ref_axis',(0.,0.,1.));
#27698=DIRECTION('',(1.,0.,0.));
#27699=DIRECTION('center_axis',(-1.,0.,0.));
#27700=DIRECTION('ref_axis',(0.,0.,1.));
#27701=DIRECTION('center_axis',(-1.,0.,0.));
#27702=DIRECTION('ref_axis',(0.,0.,1.));
#27703=DIRECTION('center_axis',(-1.,0.,0.));
#27704=DIRECTION('ref_axis',(0.,0.,1.));
#27705=DIRECTION('center_axis',(-1.,0.,0.));
#27706=DIRECTION('ref_axis',(0.,0.,1.));
#27707=DIRECTION('',(1.,0.,0.));
#27708=DIRECTION('center_axis',(-1.,0.,0.));
#27709=DIRECTION('ref_axis',(0.,0.,1.));
#27710=DIRECTION('center_axis',(1.,0.,0.));
#27711=DIRECTION('ref_axis',(0.,0.,-1.));
#27712=DIRECTION('',(-0.70710678118657,8.65956056235465E-17,-0.707106781186525));
#27713=DIRECTION('center_axis',(-1.,0.,0.));
#27714=DIRECTION('ref_axis',(0.,0.,1.));
#27715=DIRECTION('center_axis',(-1.,0.,0.));
#27716=DIRECTION('ref_axis',(0.,0.,1.));
#27717=DIRECTION('center_axis',(1.,0.,0.));
#27718=DIRECTION('ref_axis',(0.,0.,-1.));
#27719=DIRECTION('center_axis',(1.,0.,0.));
#27720=DIRECTION('ref_axis',(0.,0.,-1.));
#27721=DIRECTION('center_axis',(-1.,0.,0.));
#27722=DIRECTION('ref_axis',(0.,0.,1.));
#27723=DIRECTION('center_axis',(-1.,0.,0.));
#27724=DIRECTION('ref_axis',(0.,0.,1.));
#27725=DIRECTION('center_axis',(-1.,0.,0.));
#27726=DIRECTION('ref_axis',(0.,5.66553889764798E-16,-1.));
#27727=DIRECTION('center_axis',(-1.,0.,0.));
#27728=DIRECTION('ref_axis',(0.,0.,1.));
#27729=DIRECTION('center_axis',(-1.,0.,0.));
#27730=DIRECTION('ref_axis',(0.,0.,1.));
#27731=DIRECTION('',(0.,0.,1.));
#27732=DIRECTION('',(0.,1.,1.44560289664734E-16));
#27733=DIRECTION('',(0.,-2.4093381610789E-16,1.));
#27734=DIRECTION('center_axis',(1.,0.,0.));
#27735=DIRECTION('ref_axis',(0.,0.,-1.));
#27736=DIRECTION('center_axis',(0.,1.,0.));
#27737=DIRECTION('ref_axis',(0.,0.,1.));
#27738=DIRECTION('',(0.,0.,-1.));
#27739=DIRECTION('',(1.,0.,0.));
#27740=DIRECTION('center_axis',(0.,-1.,-2.4093381610789E-16));
#27741=DIRECTION('ref_axis',(0.,2.4093381610789E-16,-1.));
#27742=DIRECTION('',(1.,0.,0.));
#27743=DIRECTION('',(0.,-2.4093381610789E-16,1.));
#27744=DIRECTION('center_axis',(0.,1.44560289664734E-16,-1.));
#27745=DIRECTION('ref_axis',(0.,1.,1.44560289664734E-16));
#27746=DIRECTION('center_axis',(0.,-1.44560289664734E-16,1.));
#27747=DIRECTION('ref_axis',(0.,1.,1.44560289664734E-16));
#27748=DIRECTION('center_axis',(0.,0.,1.));
#27749=DIRECTION('ref_axis',(-1.,1.22464679914735E-16,0.));
#34770=CARTESIAN_POINT('',(0.,0.,0.));
#34771=CARTESIAN_POINT('Origin',(-7.49999999999999,0.,0.));
#34772=CARTESIAN_POINT('',(385.2,-6.12323399573687E-16,-5.00000000000009));
#34773=CARTESIAN_POINT('Origin',(385.2,0.,0.));
#34774=CARTESIAN_POINT('',(399.5,-6.12323399573687E-16,-5.00000000000009));
#34775=CARTESIAN_POINT('',(-7.49999999999999,-6.12323399573687E-16,-5.00000000000009));
#34776=CARTESIAN_POINT('',(399.5,-1.5,4.76969600708481));
#34777=CARTESIAN_POINT('Origin',(399.5,0.,0.));
#34778=CARTESIAN_POINT('',(389.5,-1.5,4.76969600708482));
#34779=CARTESIAN_POINT('',(-7.49999999999999,-1.5,4.76969600708482));
#34780=CARTESIAN_POINT('',(389.5,1.5,4.76969600708482));
#34781=CARTESIAN_POINT('Ctrl Pts',(389.5,1.5,4.76969600708482));
#34782=CARTESIAN_POINT('Ctrl Pts',(389.310361373005,1.5,4.76969600708482));
#34783=CARTESIAN_POINT('Ctrl Pts',(389.108946257286,1.46186045804959,4.78218969528753));
#34784=CARTESIAN_POINT('Ctrl Pts',(388.739762231142,1.30843336307885,4.82642478051612));
#34785=CARTESIAN_POINT('Ctrl Pts',(388.571882312748,1.19320265630731,4.85743375864517));
#34786=CARTESIAN_POINT('Ctrl Pts',(388.306836828799,0.928157172358542,4.914967813075));
#34787=CARTESIAN_POINT('Ctrl Pts',(388.191575546484,0.760261209503116,4.94535597495049));
#34788=CARTESIAN_POINT('Ctrl Pts',(388.038125876745,0.391018858740931,4.98815066693925));
#34789=CARTESIAN_POINT('Ctrl Pts',(388.,0.189582132646001,5.00000000000009));
#34790=CARTESIAN_POINT('Ctrl Pts',(388.,-0.189582132646003,5.00000000000009));
#34791=CARTESIAN_POINT('Ctrl Pts',(388.038125876745,-0.391018858740932,
4.98815066693925));
#34792=CARTESIAN_POINT('Ctrl Pts',(388.191575546484,-0.760261209503118,
4.94535597495048));
#34793=CARTESIAN_POINT('Ctrl Pts',(388.306836828799,-0.928157172358544,
4.914967813075));
#34794=CARTESIAN_POINT('Ctrl Pts',(388.571882312748,-1.19320265630731,4.85743375864517));
#34795=CARTESIAN_POINT('Ctrl Pts',(388.739762231142,-1.30843336307885,4.82642478051612));
#34796=CARTESIAN_POINT('Ctrl Pts',(389.108946257286,-1.4618604580496,4.78218969528753));
#34797=CARTESIAN_POINT('Ctrl Pts',(389.310361373005,-1.5,4.76969600708482));
#34798=CARTESIAN_POINT('Ctrl Pts',(389.5,-1.5,4.76969600708482));
#34799=CARTESIAN_POINT('',(399.5,1.5,4.76969600708481));
#34800=CARTESIAN_POINT('',(-7.49999999999999,1.5,4.76969600708482));
#34801=CARTESIAN_POINT('Origin',(399.5,0.,0.));
#34802=CARTESIAN_POINT('Origin',(385.2,0.,0.));
#34803=CARTESIAN_POINT('',(385.,-6.36816335556636E-16,-5.2000000000001));
#34804=CARTESIAN_POINT('Origin',(385.,0.,0.));
#34805=CARTESIAN_POINT('Origin',(385.2,-6.36816335556636E-16,-5.2000000000001));
#34806=CARTESIAN_POINT('Origin',(385.,0.,0.));
#34807=CARTESIAN_POINT('',(384.5,-7.34788079488421E-16,-6.00000000000007));
#34808=CARTESIAN_POINT('Origin',(384.5,0.,0.));
#34809=CARTESIAN_POINT('',(385.,-6.73555739531045E-16,-5.50000000000001));
#34810=CARTESIAN_POINT('',(385.,-6.73555739531045E-16,-5.50000000000001));
#34811=CARTESIAN_POINT('Origin',(385.,0.,0.));
#34812=CARTESIAN_POINT('Origin',(-7.49999999999999,0.,0.));
#34813=CARTESIAN_POINT('',(346.3,-7.34788079488418E-16,-6.00000000000005));
#34814=CARTESIAN_POINT('Origin',(346.3,0.,0.));
#34815=CARTESIAN_POINT('',(-7.49999999999999,-7.34788079488418E-16,-6.00000000000005));
#34816=CARTESIAN_POINT('Origin',(346.3,0.,0.));
#34817=CARTESIAN_POINT('',(346.,-7.71527483462834E-16,-6.30000000000001));
#34818=CARTESIAN_POINT('Origin',(346.,0.,0.));
#34819=CARTESIAN_POINT('Origin',(346.3,-7.71527483462834E-16,-6.30000000000001));
#34820=CARTESIAN_POINT('Origin',(346.,0.,0.));
#34821=CARTESIAN_POINT('',(345.5,-9.18485099360533E-16,-7.50000000000014));
#34822=CARTESIAN_POINT('Origin',(345.5,0.,0.));
#34823=CARTESIAN_POINT('',(346.,-8.57252759403155E-16,-7.00000000000006));
#34824=CARTESIAN_POINT('',(346.,-8.57252759403155E-16,-7.00000000000006));
#34825=CARTESIAN_POINT('Origin',(346.,0.,0.));
#34826=CARTESIAN_POINT('Origin',(-7.49999999999999,0.,0.));
#34827=CARTESIAN_POINT('',(11.5,9.18485099360514E-16,7.49999999999999));
#34828=CARTESIAN_POINT('',(11.5,-9.1848509936052E-16,-7.50000000000004));
#34829=CARTESIAN_POINT('Origin',(11.5,0.,0.));
#34830=CARTESIAN_POINT('Origin',(11.5,0.,0.));
#34831=CARTESIAN_POINT('',(-7.49999999999999,-9.1848509936052E-16,-7.50000000000004));
#34832=CARTESIAN_POINT('Origin',(11.5,0.,0.));
#34833=CARTESIAN_POINT('',(11.,-8.5725275940315E-16,7.00000000000002));
#34834=CARTESIAN_POINT('',(11.5,-9.18485099360514E-16,7.49999999999999));
#34835=CARTESIAN_POINT('Origin',(11.,0.,0.));
#34836=CARTESIAN_POINT('Origin',(10.7,0.,0.));
#34837=CARTESIAN_POINT('',(10.7,-6.12323399573677E-16,-5.));
#34838=CARTESIAN_POINT('Origin',(10.7,0.,0.));
#34839=CARTESIAN_POINT('',(11.,-6.49062803548097E-16,-5.3));
#34840=CARTESIAN_POINT('Origin',(10.7,-6.49062803548097E-16,-5.3));
#34841=CARTESIAN_POINT('Origin',(11.,0.,0.));
#34842=CARTESIAN_POINT('Origin',(-7.49999999999999,0.,0.));
#34843=CARTESIAN_POINT('',(3.00000000000001,-6.12323399573677E-16,-5.));
#34844=CARTESIAN_POINT('Origin',(3.00000000000001,0.,0.));
#34845=CARTESIAN_POINT('',(-7.49999999999999,-6.12323399573677E-16,-5.));
#34846=CARTESIAN_POINT('Origin',(-7.49999999999999,0.,0.));
#34847=CARTESIAN_POINT('',(1.85000000000001,-5.87830463590729E-16,-4.8));
#34848=CARTESIAN_POINT('Origin',(1.85000000000001,0.,0.));
#34849=CARTESIAN_POINT('',(3.00000000000001,-5.87830463590729E-16,-4.8));
#34850=CARTESIAN_POINT('',(-7.49999999999999,-5.87830463590729E-16,-4.8));
#34851=CARTESIAN_POINT('Origin',(3.00000000000001,0.,0.));
#34852=CARTESIAN_POINT('Origin',(-7.49999999999999,0.,0.));
#34853=CARTESIAN_POINT('',(0.5,6.12323399573677E-16,5.));
#34854=CARTESIAN_POINT('',(0.5,-6.12323399573677E-16,-5.));
#34855=CARTESIAN_POINT('Origin',(0.5,0.,0.));
#34856=CARTESIAN_POINT('Origin',(0.5,0.,0.));
#34857=CARTESIAN_POINT('',(1.85000000000001,-6.12323399573677E-16,-5.));
#34858=CARTESIAN_POINT('',(-7.49999999999999,-6.12323399573677E-16,-5.));
#34859=CARTESIAN_POINT('Origin',(1.85000000000001,0.,0.));
#34860=CARTESIAN_POINT('Origin',(0.5,0.,0.));
#34861=CARTESIAN_POINT('',(6.93889390390723E-17,-5.51091059616313E-16,4.50000000000003));
#34862=CARTESIAN_POINT('',(0.5,-6.12323399573677E-16,5.));
#34863=CARTESIAN_POINT('Origin',(0.,0.,0.));
#34864=CARTESIAN_POINT('Origin',(1.85000000000001,5.,0.));
#34865=CARTESIAN_POINT('Origin',(3.00000000000001,5.,0.));
#34866=CARTESIAN_POINT('Origin',(11.,7.00000000000002,0.));
#34867=CARTESIAN_POINT('Origin',(346.,6.30000000000001,0.));
#34868=CARTESIAN_POINT('Origin',(385.,5.2000000000001,0.));
#34869=CARTESIAN_POINT('Origin',(400.,0.,0.));
#34870=CARTESIAN_POINT('',(400.,1.5,4.24264068711934));
#34871=CARTESIAN_POINT('Ctrl Pts',(399.5,1.5,4.76969600708481));
#34872=CARTESIAN_POINT('Ctrl Pts',(399.66715123186,1.5,4.59447390528654));
#34873=CARTESIAN_POINT('Ctrl Pts',(399.833884933644,1.5,4.41883232193548));
#34874=CARTESIAN_POINT('Ctrl Pts',(400.,1.5,4.24264068711934));
#34875=CARTESIAN_POINT('',(400.,-1.5,4.24264068711934));
#34876=CARTESIAN_POINT('Origin',(400.,0.,0.));
#34877=CARTESIAN_POINT('Ctrl Pts',(400.,-1.5,4.24264068711934));
#34878=CARTESIAN_POINT('Ctrl Pts',(399.833876215866,-1.5,4.41884156853607));
#34879=CARTESIAN_POINT('Ctrl Pts',(399.667149605032,-1.5,4.59447561066608));
#34880=CARTESIAN_POINT('Ctrl Pts',(399.5,-1.5,4.76969600708481));
#34881=CARTESIAN_POINT('Origin',(400.,0.,0.));
#34882=CARTESIAN_POINT('',(400.,1.5,3.2));
#34883=CARTESIAN_POINT('',(400.,1.5,5.));
#34884=CARTESIAN_POINT('',(400.,-1.5,3.2));
#34885=CARTESIAN_POINT('',(400.,1.5,3.2));
#34886=CARTESIAN_POINT('',(400.,-1.5,-3.61400724161835E-16));
#34887=CARTESIAN_POINT('Origin',(2.14313189850789E-16,4.50000000000003,
0.));
#34888=CARTESIAN_POINT('Origin',(388.,1.5,5.));
#34889=CARTESIAN_POINT('',(389.5,1.5,3.2));
#34890=CARTESIAN_POINT('',(389.5,1.5,5.));
#34891=CARTESIAN_POINT('',(388.,1.5,3.2));
#34892=CARTESIAN_POINT('Origin',(388.,-1.5,5.));
#34893=CARTESIAN_POINT('',(389.5,-1.5,3.2));
#34894=CARTESIAN_POINT('',(388.,-1.5,3.2));
#34895=CARTESIAN_POINT('',(389.5,-1.5,5.));
#34896=CARTESIAN_POINT('Origin',(388.,1.5,3.2));
#34897=CARTESIAN_POINT('Origin',(389.5,-6.50521303491303E-16,3.2));
#34898=CARTESIAN_POINT('Origin',(389.5,-6.50521303491303E-16,0.));
#57006=UNCERTAINTY_MEASURE_WITH_UNIT(LENGTH_MEASURE(0.01),#57080,
'DISTANCE_ACCURACY_VALUE',
'Maximum model space distance between geometric entities at asserted c
onnectivities');
#57040=UNCERTAINTY_MEASURE_WITH_UNIT(LENGTH_MEASURE(0.01),#57080,
'DISTANCE_ACCURACY_VALUE',
'Maximum model space distance between geometric entities at asserted c
onnectivities');
#57045=(
GEOMETRIC_REPRESENTATION_CONTEXT(3)
GLOBAL_UNCERTAINTY_ASSIGNED_CONTEXT((#57006))
GLOBAL_UNIT_ASSIGNED_CONTEXT((#57080,#57082,#57083))
REPRESENTATION_CONTEXT('','3D')
);
#57079=(
GEOMETRIC_REPRESENTATION_CONTEXT(3)
GLOBAL_UNCERTAINTY_ASSIGNED_CONTEXT((#57040))
GLOBAL_UNIT_ASSIGNED_CONTEXT((#57080,#57082,#57083))
REPRESENTATION_CONTEXT('','3D')
);
#57080=(
LENGTH_UNIT()
NAMED_UNIT(*)
SI_UNIT(.MILLI.,.METRE.)
);
#57082=(
NAMED_UNIT(*)
PLANE_ANGLE_UNIT()
SI_UNIT($,.RADIAN.)
);
#57083=(
NAMED_UNIT(*)
SI_UNIT($,.STERADIAN.)
SOLID_ANGLE_UNIT()
);
#57088=SHAPE_DEFINITION_REPRESENTATION(#57126,#57253);
#57126=PRODUCT_DEFINITION_SHAPE('',$,#57292);
#57253=SHAPE_REPRESENTATION('',(#24937),#57045);
#57287=PRODUCT_DEFINITION_CONTEXT('part definition',#57403,'design');
#57292=PRODUCT_DEFINITION('Ball Screw Shaft','Ball Screw Shaft',#57330,
#57287);
#57330=PRODUCT_DEFINITION_FORMATION('',$,#57409);
#57403=APPLICATION_CONTEXT(
'Core Data for Automotive Mechanical Design Process');
#57404=PRODUCT_CONTEXT('part definition',#57403,'mechanical');
#57409=PRODUCT('Ball Screw Shaft','Ball Screw Shaft',$,(#57404));
#57444=PRESENTATION_STYLE_ASSIGNMENT((#57446));
#57446=SURFACE_STYLE_USAGE(.BOTH.,#57448);
#57448=SURFACE_SIDE_STYLE('',(#57450));
#57450=SURFACE_STYLE_FILL_AREA(#57452);
#57452=FILL_AREA_STYLE('Opaque(202,209,238)',(#57454));
#57454=FILL_AREA_STYLE_COLOUR('Opaque(202,209,238)',#57456);
#57456=COLOUR_RGB('Opaque(202,209,238)',0.792156862745098,0.819607843137255,
0.933333333333333);
ENDSEC;
END-ISO-10303-21;
